ISO-10303-21;
HEADER;
/* Generated by software containing ST-Developer
 * from STEP Tools, Inc. (www.steptools.com) 
 */

FILE_DESCRIPTION(
/* description */ ('Line shaft on three pillow blocks'),
/* implementation_level */ '2;1');

FILE_NAME(
/* name */ 'Mounting reducer bush (4).step',
/* time_stamp */ '2026-10-27T10:49:19-07:00',
/* author */ (''),
/* organization */ (''),
/* preprocessor_version */ 'ST-DEVELOPER v20.2',
/* originating_system */ 'Autodesk Translation Framework v15.17.0.0',
/* authorisation */ '');

FILE_SCHEMA (('AUTOMOTIVE_DESIGN { 1 0 10303 214 3 1 1 }'));
ENDSEC;

DATA;
#10=MECHANICAL_DESIGN_GEOMETRIC_PRESENTATION_REPRESENTATION('',(#347),#8377);
#293=SHAPE_REPRESENTATION_RELATIONSHIP('SRR','None',#8508,#320);
#320=ADVANCED_BREP_SHAPE_REPRESENTATION('',(#375),#8357);
#347=STYLED_ITEM('',(#8732),#375);
#375=MANIFOLD_SOLID_BREP('Body1',#4333);
#423=FACE_BOUND('',#1005,.T.);
#424=FACE_BOUND('',#1007,.T.);
#530=PLANE('',#4779);
#531=PLANE('',#4780);
#718=FACE_OUTER_BOUND('',#1002,.T.);
#719=FACE_OUTER_BOUND('',#1003,.T.);
#720=FACE_OUTER_BOUND('',#1004,.T.);
#721=FACE_OUTER_BOUND('',#1006,.T.);
#1002=EDGE_LOOP('',(#3201,#3202,#3203,#3204));
#1003=EDGE_LOOP('',(#3205,#3206,#3207,#3208));
#1004=EDGE_LOOP('',(#3209));
#1005=EDGE_LOOP('',(#3210));
#1006=EDGE_LOOP('',(#3211));
#1007=EDGE_LOOP('',(#3212));
#1337=LINE('',#6755,#1664);
#1338=LINE('',#6761,#1665);
#1664=VECTOR('',#5474,0.425);
#1665=VECTOR('',#5481,0.645);
#1953=CIRCLE('',#4774,0.425);
#1954=CIRCLE('',#4775,0.425);
#1955=CIRCLE('',#4777,0.645);
#1956=CIRCLE('',#4778,0.645);
#2152=VERTEX_POINT('',#6752);
#2153=VERTEX_POINT('',#6754);
#2154=VERTEX_POINT('',#6758);
#2155=VERTEX_POINT('',#6760);
#2549=EDGE_CURVE('',#2152,#2152,#1953,.T.);
#2550=EDGE_CURVE('',#2152,#2153,#1337,.T.);
#2551=EDGE_CURVE('',#2153,#2153,#1954,.T.);
#2552=EDGE_CURVE('',#2154,#2154,#1955,.T.);
#2553=EDGE_CURVE('',#2154,#2155,#1338,.T.);
#2554=EDGE_CURVE('',#2155,#2155,#1956,.T.);
#3201=ORIENTED_EDGE('',*,*,#2549,.F.);
#3202=ORIENTED_EDGE('',*,*,#2550,.T.);
#3203=ORIENTED_EDGE('',*,*,#2551,.T.);
#3204=ORIENTED_EDGE('',*,*,#2550,.F.);
#3205=ORIENTED_EDGE('',*,*,#2552,.F.);
#3206=ORIENTED_EDGE('',*,*,#2553,.T.);
#3207=ORIENTED_EDGE('',*,*,#2554,.T.);
#3208=ORIENTED_EDGE('',*,*,#2553,.F.);
#3209=ORIENTED_EDGE('',*,*,#2552,.T.);
#3210=ORIENTED_EDGE('',*,*,#2549,.T.);
#3211=ORIENTED_EDGE('',*,*,#2554,.F.);
#3212=ORIENTED_EDGE('',*,*,#2551,.F.);
#4023=CYLINDRICAL_SURFACE('',#4773,0.425);
#4024=CYLINDRICAL_SURFACE('',#4776,0.645);
#4136=ADVANCED_FACE('',(#718),#4023,.F.);
#4137=ADVANCED_FACE('',(#719),#4024,.T.);
#4138=ADVANCED_FACE('',(#720,#423),#530,.T.);
#4139=ADVANCED_FACE('',(#721,#424),#531,.F.);
#4333=CLOSED_SHELL('',(#4136,#4137,#4138,#4139));
#4772=AXIS2_PLACEMENT_3D('',#6750,#5468,#5469);
#4773=AXIS2_PLACEMENT_3D('',#6751,#5470,#5471);
#4774=AXIS2_PLACEMENT_3D('',#6753,#5472,#5473);
#4775=AXIS2_PLACEMENT_3D('',#6756,#5475,#5476);
#4776=AXIS2_PLACEMENT_3D('',#6757,#5477,#5478);
#4777=AXIS2_PLACEMENT_3D('',#6759,#5479,#5480);
#4778=AXIS2_PLACEMENT_3D('',#6762,#5482,#5483);
#4779=AXIS2_PLACEMENT_3D('',#6763,#5484,#5485);
#4780=AXIS2_PLACEMENT_3D('',#6764,#5486,#5487);
#5468=DIRECTION('axis',(0.,0.,1.));
#5469=DIRECTION('refdir',(1.,0.,0.));
#5470=DIRECTION('center_axis',(0.,0.,1.));
#5471=DIRECTION('ref_axis',(1.,0.,0.));
#5472=DIRECTION('center_axis',(0.,0.,-1.));
#5473=DIRECTION('ref_axis',(1.,0.,0.));
#5474=DIRECTION('',(0.,0.,-1.));
#5475=DIRECTION('center_axis',(0.,0.,-1.));
#5476=DIRECTION('ref_axis',(1.,0.,0.));
#5477=DIRECTION('center_axis',(0.,0.,1.));
#5478=DIRECTION('ref_axis',(1.,0.,0.));
#5479=DIRECTION('center_axis',(0.,0.,1.));
#5480=DIRECTION('ref_axis',(1.,0.,0.));
#5481=DIRECTION('',(0.,0.,-1.));
#5482=DIRECTION('center_axis',(0.,0.,1.));
#5483=DIRECTION('ref_axis',(1.,0.,0.));
#5484=DIRECTION('center_axis',(0.,0.,1.));
#5485=DIRECTION('ref_axis',(1.,0.,0.));
#5486=DIRECTION('center_axis',(0.,0.,1.));
#5487=DIRECTION('ref_axis',(1.,0.,0.));
#6750=CARTESIAN_POINT('',(0.,0.,0.));
#6751=CARTESIAN_POINT('Origin',(-4.75,30.,1.2));
#6752=CARTESIAN_POINT('',(-5.175,30.,2.4));
#6753=CARTESIAN_POINT('Origin',(-4.75,30.,2.4));
#6754=CARTESIAN_POINT('',(-5.175,30.,1.2));
#6755=CARTESIAN_POINT('',(-5.175,30.,1.2));
#6756=CARTESIAN_POINT('Origin',(-4.75,30.,1.2));
#6757=CARTESIAN_POINT('Origin',(-4.75,30.,1.2));
#6758=CARTESIAN_POINT('',(-5.395,30.,2.4));
#6759=CARTESIAN_POINT('Origin',(-4.75,30.,2.4));
#6760=CARTESIAN_POINT('',(-5.395,30.,1.2));
#6761=CARTESIAN_POINT('',(-5.395,30.,1.2));
#6762=CARTESIAN_POINT('Origin',(-4.75,30.,1.2));
#6763=CARTESIAN_POINT('Origin',(-4.75,30.,2.4));
#6764=CARTESIAN_POINT('Origin',(-4.75,30.,1.2));
#8325=UNCERTAINTY_MEASURE_WITH_UNIT(LENGTH_MEASURE(0.001),#8378,
'DISTANCE_ACCURACY_VALUE',
'Maximum model space distance between geometric entities at asserted c
onnectivities');
#8345=UNCERTAINTY_MEASURE_WITH_UNIT(LENGTH_MEASURE(0.001),#8378,
'DISTANCE_ACCURACY_VALUE',
'Maximum model space distance between geometric entities at asserted c
onnectivities');
#8357=(
GEOMETRIC_REPRESENTATION_CONTEXT(3)
GLOBAL_UNCERTAINTY_ASSIGNED_CONTEXT((#8325))
GLOBAL_UNIT_ASSIGNED_CONTEXT((#8378,#8380,#8381))
REPRESENTATION_CONTEXT('','3D')
);
#8377=(
GEOMETRIC_REPRESENTATION_CONTEXT(3)
GLOBAL_UNCERTAINTY_ASSIGNED_CONTEXT((#8345))
GLOBAL_UNIT_ASSIGNED_CONTEXT((#8378,#8380,#8381))
REPRESENTATION_CONTEXT('','3D')
);
#8378=(
LENGTH_UNIT()
NAMED_UNIT(*)
SI_UNIT(.CENTI.,.METRE.)
);
#8380=(
NAMED_UNIT(*)
PLANE_ANGLE_UNIT()
SI_UNIT($,.RADIAN.)
);
#8381=(
NAMED_UNIT(*)
SI_UNIT($,.STERADIAN.)
SOLID_ANGLE_UNIT()
);
#8393=SHAPE_DEFINITION_REPRESENTATION(#8424,#8508);
#8424=PRODUCT_DEFINITION_SHAPE('',$,#8540);
#8508=SHAPE_REPRESENTATION('',(#4772),#8357);
#8528=PRODUCT_DEFINITION_CONTEXT('part definition',#8623,'design');
#8540=PRODUCT_DEFINITION('Mounting reducer bush (4)',
'Mounting reducer bush (4)',#8571,#8528);
#8571=PRODUCT_DEFINITION_FORMATION('',$,#8636);
#8623=APPLICATION_CONTEXT(
'Core Data for Automotive Mechanical Design Process');
#8624=PRODUCT_CONTEXT('part definition',#8623,'mechanical');
#8636=PRODUCT('Mounting reducer bush (4)','Mounting reducer bush (4)',
'Mounting reducer bush (4)',(#8624));
#8726=COLOUR_RGB('Off White',0.89,0.88,0.83);
#8727=FILL_AREA_STYLE_COLOUR('',#8726);
#8728=FILL_AREA_STYLE('',(#8727));
#8729=SURFACE_STYLE_FILL_AREA(#8728);
#8730=SURFACE_SIDE_STYLE('',(#8729));
#8731=SURFACE_STYLE_USAGE(.BOTH.,#8730);
#8732=PRESENTATION_STYLE_ASSIGNMENT((#8731));
ENDSEC;
END-ISO-10303-21;
